ISO-10303-21;
HEADER;
FILE_DESCRIPTION (('STEP AP214'),
    '1' );
FILE_NAME ('socket head cap screw_iso_ISO 4762 M5 x 35 - 22N.step',
    '2026-09-24T10:28:59',
    ( '' ),
    ( '' ),
    'SwSTEP 2.0',
    'SolidWorks 2026',
    '' );
FILE_SCHEMA (( 'AUTOMOTIVE_DESIGN' ));
ENDSEC;

DATA;
#5=LINE ( 'NONE', #2469, #13948 ) ;
#147=ADVANCED_FACE ( 'NONE', ( #12333 ), #17898, .T. ) ;
#158=DIRECTION ( 'NONE',  ( -1.000000000000000000, -0.000000000000000000, -0.000000000000000000 ) ) ;
#171=ORIENTED_EDGE ( 'NONE', *, *, #13786, .T. ) ;
#199=DIRECTION ( 'NONE',  ( 0.000000000000000000, -1.000000000000000000, 0.000000000000000000 ) ) ;
#216=AXIS2_PLACEMENT_3D ( 'NONE', #2816, #4451, #10954 ) ;
#232=DIRECTION ( 'NONE',  ( 0.000000000000000000, 0.000000000000000000, -1.000000000000000000 ) ) ;
#239=ORIENTED_EDGE ( 'NONE', *, *, #8844, .T. ) ;
#254=VERTEX_POINT ( 'NONE', #16603 ) ;
#264=CIRCLE ( 'NONE', #10381, 4.250000000000000000 ) ;
#272=CARTESIAN_POINT ( 'NONE',  ( 0.000000000000000000, -1.178949249685218081, -2.041999999999998039 ) ) ;
#280=CARTESIAN_POINT ( 'NONE',  ( 5.200000000000002842, 0.000000000000000000, 2.500000000000000444 ) ) ;
#312=CLOSED_SHELL ( 'NONE', ( #13052, #4033, #17691, #12015, #10916, #12800, #4306, #10100, #2178, #4714, #3417, #147, #13494, #15586, #15060, #10969, #7511, #8648, #5633, #10348, #2026, #9611, #12090, #6179, #12893, #7460, #15673 ) ) ;
#328=DIRECTION ( 'NONE',  ( 1.000000000000000000, 0.000000000000000000, 0.000000000000000000 ) ) ;
#345=FILL_AREA_STYLE ('',( #12748 ) ) ;
#392=ORIENTED_EDGE ( 'NONE', *, *, #2514, .T. ) ;
#395=ORIENTED_EDGE ( 'NONE', *, *, #4966, .T. ) ;
#473=EDGE_LOOP ( 'NONE', ( #2498, #12388, #7781 ) ) ;
#558=VERTEX_POINT ( 'NONE', #17253 ) ;
#561=VECTOR ( 'NONE', #15631, 1000.000000000000114 ) ;
#568=ORIENTED_EDGE ( 'NONE', *, *, #9077, .T. ) ;
#587=CARTESIAN_POINT ( 'NONE',  ( 39.99999999999999289, 2.516649172247811061E-16, -2.055000000000000160 ) ) ;
#594=CIRCLE ( 'NONE', #15644, 2.500000000000000444 ) ;
#626=AXIS2_PLACEMENT_3D ( 'NONE', #4264, #16880, #2897 ) ;
#638=UNCERTAINTY_MEASURE_WITH_UNIT (LENGTH_MEASURE( 1.000000000000000082E-05 ), #792, 'distance_accuracy_value', 'NONE');
#653=VECTOR ( 'NONE', #15551, 1000.000000000000000 ) ;
#675=DIRECTION ( 'NONE',  ( 0.000000000000000000, 0.000000000000000000, 1.000000000000000000 ) ) ;
#705=DIRECTION ( 'NONE',  ( 0.000000000000000000, 1.000000000000000000, -1.287488025362403787E-15 ) ) ;
#741=CARTESIAN_POINT ( 'NONE',  ( 2.500000000000000000, 2.357898499370432166, -2.385244779468109755E-15 ) ) ;
#748=PLANE ( 'NONE',  #4098 ) ;
#791=LINE ( 'NONE', #6320, #11242 ) ;
#792=( LENGTH_UNIT ( ) NAMED_UNIT ( * ) SI_UNIT ( .MILLI., .METRE. ) );
#817=PRODUCT_DEFINITION ( 'UNKNOWN', '', #4819, #12962 ) ;
#865=CIRCLE ( 'NONE', #10967, 4.250000000000000000 ) ;
#867=VECTOR ( 'NONE', #15936, 1000.000000000000000 ) ;
#908=ORIENTED_EDGE ( 'NONE', *, *, #9380, .T. ) ;
#975=ORIENTED_EDGE ( 'NONE', *, *, #1009, .F. ) ;
#979=( LENGTH_UNIT ( ) NAMED_UNIT ( * ) SI_UNIT ( .MILLI., .METRE. ) );
#1009=EDGE_CURVE ( 'NONE', #5050, #17268, #3521, .T. ) ;
#1086=ORIENTED_EDGE ( 'NONE', *, *, #10347, .F. ) ;
#1117=ORIENTED_EDGE ( 'NONE', *, *, #17232, .F. ) ;
#1182=CARTESIAN_POINT ( 'NONE',  ( 5.200000000000002842, 0.000000000000000000, 0.000000000000000000 ) ) ;
#1219=AXIS2_PLACEMENT_3D ( 'NONE', #3482, #3148, #675 ) ;
#1223=AXIS2_PLACEMENT_3D ( 'NONE', #1707, #3242, #10293 ) ;
#1225=VECTOR ( 'NONE', #2570, 1000.000000000000000 ) ;
#1248=DIRECTION ( 'NONE',  ( 0.000000000000000000, 0.4999999999999992784, -0.8660254037844390407 ) ) ;
#1252=EDGE_CURVE ( 'NONE', #2160, #254, #5493, .T. ) ;
#1285=DIRECTION ( 'NONE',  ( -1.000000000000000000, -0.000000000000000000, -0.000000000000000000 ) ) ;
#1359=LINE ( 'NONE', #11033, #2838 ) ;
#1481=EDGE_CURVE ( 'NONE', #9378, #15303, #17106, .T. ) ;
#1507=PLANE ( 'NONE',  #10112 ) ;
#1519=AXIS2_PLACEMENT_3D ( 'NONE', #14020, #16652, #3133 ) ;
#1558=CARTESIAN_POINT ( 'NONE',  ( 0.2500000000000002220, 4.898587196589412829E-16, -4.000000000000000000 ) ) ;
#1589=ORIENTED_EDGE ( 'NONE', *, *, #12669, .T. ) ;
#1595=VERTEX_POINT ( 'NONE', #14353 ) ;
#1605=COLOUR_RGB ( '', 0.09019608, 0.27058824, 0.51372549) ;
#1707=CARTESIAN_POINT ( 'NONE',  ( 0.2500000000000002220, 0.000000000000000000, 0.000000000000000000 ) ) ;
#1719=ORIENTED_EDGE ( 'NONE', *, *, #14326, .F. ) ;
#1758=DIRECTION ( 'NONE',  ( 0.000000000000000000, 0.000000000000000000, 1.000000000000000000 ) ) ;
#1764=EDGE_LOOP ( 'NONE', ( #11987, #7396, #5644, #9866, #15153 ) ) ;
#1766=CIRCLE ( 'NONE', #17732, 2.500000000000000888 ) ;
#1806=CARTESIAN_POINT ( 'NONE',  ( 2.500000000000000000, 0.000000000000000000, 0.000000000000000000 ) ) ;
#1811=CARTESIAN_POINT ( 'NONE',  ( 2.500000000000000000, 2.500728763858895382E-16, -2.041999999999999815 ) ) ;
#1819=VERTEX_POINT ( 'NONE', #9425 ) ;
#1821=CARTESIAN_POINT ( 'NONE',  ( 39.99999999999999289, 0.000000000000000000, 2.055000000000000160 ) ) ;
#1824=EDGE_CURVE ( 'NONE', #17674, #12357, #5, .T. ) ;
#1866=LINE ( 'NONE', #11348, #561 ) ;
#1873=ORIENTED_EDGE ( 'NONE', *, *, #9077, .F. ) ;
#1880=EDGE_CURVE ( 'NONE', #12037, #17674, #9682, .T. ) ;
#1920=PLANE ( 'NONE',  #14245 ) ;
#1940=CARTESIAN_POINT ( 'NONE',  ( 2.500000000000000000, 2.357898499370432166, -2.385244779468109755E-15 ) ) ;
#1944=CARTESIAN_POINT ( 'NONE',  ( 0.000000000000000000, 0.000000000000000000, 0.000000000000000000 ) ) ;
#1955=CARTESIAN_POINT ( 'NONE',  ( 5.200000000000002842, 0.000000000000000000, 0.000000000000000000 ) ) ;
#2011=DIRECTION ( 'NONE',  ( 1.000000000000000000, 0.000000000000000000, 0.000000000000000000 ) ) ;
#2022=PLANE ( 'NONE',  #14517 ) ;
#2024=ORIENTED_EDGE ( 'NONE', *, *, #16213, .F. ) ;
#2026=ADVANCED_FACE ( 'NONE', ( #13966 ), #1920, .F. ) ;
#2028=AXIS2_PLACEMENT_3D ( 'NONE', #3780, #17604, #2173 ) ;
#2102=DIRECTION ( 'NONE',  ( 0.000000000000000000, -0.5000000000000011102, -0.8660254037844379305 ) ) ;
#2155=MECHANICAL_DESIGN_GEOMETRIC_PRESENTATION_REPRESENTATION('',(#11365),#3597);
#2158=ORIENTED_EDGE ( 'NONE', *, *, #11848, .F. ) ;
#2160=VERTEX_POINT ( 'NONE', #13053 ) ;
#2173=DIRECTION ( 'NONE',  ( 0.000000000000000000, 0.000000000000000000, 1.000000000000000000 ) ) ;
#2178=ADVANCED_FACE ( 'NONE', ( #14695 ), #15693, .T. ) ;
#2293=FACE_OUTER_BOUND ( 'NONE', #16616, .T. ) ;
#2317=PRODUCT ( 'socket head cap screw_iso_ISO 4762 M5 x 35 - 22N', 'socket head cap screw_iso_ISO 4762 M5 x 35 - 22N', '', ( #5743 ) ) ;
#2330=DIRECTION ( 'NONE',  ( 0.000000000000000000, 0.000000000000000000, -1.000000000000000000 ) ) ;
#2387=DIRECTION ( 'NONE',  ( -0.5000000000000051070, 0.000000000000000000, 0.8660254037844355990 ) ) ;
#2403=VERTEX_POINT ( 'NONE', #13592 ) ;
#2423=LINE ( 'NONE', #14669, #867 ) ;
#2431=SURFACE_STYLE_FILL_AREA ( #17320 ) ;
#2449=DIRECTION ( 'NONE',  ( -1.000000000000000000, -0.000000000000000000, -0.000000000000000000 ) ) ;
#2469=CARTESIAN_POINT ( 'NONE',  ( 2.500000000000000000, -1.178949249685218081, -2.041999999999998039 ) ) ;
#2488=CARTESIAN_POINT ( 'NONE',  ( 0.2500000000000002220, 0.000000000000000000, 0.000000000000000000 ) ) ;
#2498=ORIENTED_EDGE ( 'NONE', *, *, #11162, .T. ) ;
#2511=DIRECTION ( 'NONE',  ( 0.000000000000000000, 0.5000000000000011102, 0.8660254037844380415 ) ) ;
#2513=VERTEX_POINT ( 'NONE', #4808 ) ;
#2514=EDGE_CURVE ( 'NONE', #4496, #15456, #3727, .T. ) ;
#2552=CIRCLE ( 'NONE', #6612, 2.700000000000000622 ) ;
#2559=FACE_OUTER_BOUND ( 'NONE', #6639, .T. ) ;
#2570=DIRECTION ( 'NONE',  ( 0.000000000000000000, -1.000000000000000000, 1.287488025362403787E-15 ) ) ;
#2638=LINE ( 'NONE', #12053, #5235 ) ;
#2724=ORIENTED_EDGE ( 'NONE', *, *, #11261, .T. ) ;
#2786=CARTESIAN_POINT ( 'NONE',  ( 2.500000000000000000, -1.178949249685213863, 2.042000000000001148 ) ) ;
#2815=CARTESIAN_POINT ( 'NONE',  ( 2.500000000000000000, -1.178949249685213863, 2.042000000000001148 ) ) ;
#2816=CARTESIAN_POINT ( 'NONE',  ( 5.200000000000002842, 0.000000000000000000, -2.700000000000000622 ) ) ;
#2838=VECTOR ( 'NONE', #13263, 1000.000000000000114 ) ;
#2865=ORIENTED_EDGE ( 'NONE', *, *, #16472, .T. ) ;
#2875=EDGE_LOOP ( 'NONE', ( #6703, #8241, #15202, #6122, #14011 ) ) ;
#2897=DIRECTION ( 'NONE',  ( 0.000000000000000000, 0.000000000000000000, -1.000000000000000000 ) ) ;
#2949=VECTOR ( 'NONE', #10773, 1000.000000000000000 ) ;
#2960=ORIENTED_EDGE ( 'NONE', *, *, #11162, .F. ) ;
#3031=ORIENTED_EDGE ( 'NONE', *, *, #11121, .F. ) ;
#3040=ORIENTED_EDGE ( 'NONE', *, *, #7175, .T. ) ;
#3045=CARTESIAN_POINT ( 'NONE',  ( 5.200000000000002842, 0.000000000000000000, 0.000000000000000000 ) ) ;
#3056=CARTESIAN_POINT ( 'NONE',  ( -31.74999999999995737, 0.000000000000000000, 4.250000000000000000 ) ) ;
#3063=CARTESIAN_POINT ( 'NONE',  ( 2.500000000000000000, 0.000000000000000000, 0.000000000000000000 ) ) ;
#3099=EDGE_LOOP ( 'NONE', ( #1086, #10082, #8786, #975 ) ) ;
#3107=CYLINDRICAL_SURFACE ( 'NONE', #11288, 2.500000000000000444 ) ;
#3133=DIRECTION ( 'NONE',  ( 0.000000000000000000, 0.000000000000000000, 1.000000000000000000 ) ) ;
#3135=AXIS2_PLACEMENT_3D ( 'NONE', #16840, #16558, #7048 ) ;
#3140=ORIENTED_EDGE ( 'NONE', *, *, #16607, .F. ) ;
#3148=DIRECTION ( 'NONE',  ( -1.000000000000000000, -0.000000000000000000, -0.000000000000000000 ) ) ;
#3157=EDGE_CURVE ( 'NONE', #8806, #13014, #9501, .T. ) ;
#3168=EDGE_CURVE ( 'NONE', #15953, #8806, #4403, .T. ) ;
#3188=ORIENTED_EDGE ( 'NONE', *, *, #14174, .F. ) ;
#3198=FACE_OUTER_BOUND ( 'NONE', #15405, .T. ) ;
#3212=EDGE_LOOP ( 'NONE', ( #1873, #392, #4874, #1589, #10059 ) ) ;
#3239=( LENGTH_UNIT ( ) NAMED_UNIT ( * ) SI_UNIT ( .MILLI., .METRE. ) );
#3242=DIRECTION ( 'NONE',  ( -1.000000000000000000, -0.000000000000000000, -0.000000000000000000 ) ) ;
#3314=DIRECTION ( 'NONE',  ( 0.000000000000000000, 0.000000000000000000, -1.000000000000000000 ) ) ;
#3339=SHAPE_REPRESENTATION ( 'socket head cap screw_iso_ISO 4762 M5 x 35 - 22N', ( #3575 ), #5366 ) ;
#3356=CARTESIAN_POINT ( 'NONE',  ( 39.99999999999999289, 0.000000000000000000, 0.000000000000000000 ) ) ;
#3414=CARTESIAN_POINT ( 'NONE',  ( 2.500000000000000000, 0.000000000000000000, 0.000000000000000000 ) ) ;
#3417=ADVANCED_FACE ( 'NONE', ( #17672, #9286 ), #16375, .T. ) ;
#3448=VECTOR ( 'NONE', #7975, 1000.000000000000114 ) ;
#3453=EDGE_LOOP ( 'NONE', ( #17654, #12272, #10983, #8467 ) ) ;
#3482=CARTESIAN_POINT ( 'NONE',  ( 39.99999999999999289, 0.000000000000000000, 0.000000000000000000 ) ) ;
#3489=VECTOR ( 'NONE', #15521, 1000.000000000000114 ) ;
#3521=CIRCLE ( 'NONE', #626, 2.700000000000000622 ) ;
#3575=AXIS2_PLACEMENT_3D ( 'NONE', #5095, #17575, #9272 ) ;
#3581=COLOUR_RGB ( '', 0.09019608, 0.27058824, 0.51372549) ;
#3583=FACE_OUTER_BOUND ( 'NONE', #15071, .T. ) ;
#3597=( GEOMETRIC_REPRESENTATION_CONTEXT ( 3 ) GLOBAL_UNCERTAINTY_ASSIGNED_CONTEXT ( ( #9343 ) ) GLOBAL_UNIT_ASSIGNED_CONTEXT ( ( #3239, #11743, #11832 ) ) REPRESENTATION_CONTEXT ( 'NONE', 'WORKASPACE' ) );
#3673=CARTESIAN_POINT ( 'NONE',  ( 2.500000000000000000, 2.357898499370432166, -2.385244779468109755E-15 ) ) ;
#3691=SHAPE_REPRESENTATION_RELATIONSHIP ( 'NONE' , 'NONE' ,  #3339, #5711 ) ;
#3706=LINE ( 'NONE', #13320, #13380 ) ;
#3727=LINE ( 'NONE', #11974, #17491 ) ;
#3748=ORIENTED_EDGE ( 'NONE', *, *, #9942, .F. ) ;
#3780=CARTESIAN_POINT ( 'NONE',  ( 39.55500000000002103, 0.000000000000000000, 0.000000000000000000 ) ) ;
#3829=CIRCLE ( 'NONE', #11026, 2.041999999999999815 ) ;
#3834=AXIS2_PLACEMENT_3D ( 'NONE', #3063, #158, #5491 ) ;
#3838=DIRECTION ( 'NONE',  ( 0.000000000000000000, 0.000000000000000000, 1.000000000000000000 ) ) ;
#3906=ORIENTED_EDGE ( 'NONE', *, *, #17037, .T. ) ;
#3921=CARTESIAN_POINT ( 'NONE',  ( 2.500000000000000000, 0.000000000000000000, 0.000000000000000000 ) ) ;
#3933=LINE ( 'NONE', #14984, #1225 ) ;
#4033=ADVANCED_FACE ( 'NONE', ( #6649 ), #9188, .T. ) ;
#4098=AXIS2_PLACEMENT_3D ( 'NONE', #14805, #5000, #13444 ) ;
#4110=AXIS2_PLACEMENT_3D ( 'NONE', #3921, #5440, #3838 ) ;
#4130=ORIENTED_EDGE ( 'NONE', *, *, #14174, .T. ) ;
#4150=ORIENTED_EDGE ( 'NONE', *, *, #17037, .F. ) ;
#4234=ORIENTED_EDGE ( 'NONE', *, *, #9787, .T. ) ;
#4264=CARTESIAN_POINT ( 'NONE',  ( 5.000000000000000888, 0.000000000000000000, 0.000000000000000000 ) ) ;
#4302=ORIENTED_EDGE ( 'NONE', *, *, #13999, .F. ) ;
#4305=AXIS2_PLACEMENT_3D ( 'NONE', #8952, #13126, #705 ) ;
#4306=ADVANCED_FACE ( 'NONE', ( #15620, #3198 ), #8737, .T. ) ;
#4309=DIRECTION ( 'NONE',  ( 0.000000000000000000, 0.4999999999999991118, -0.8660254037844391517 ) ) ;
#4354=AXIS2_PLACEMENT_3D ( 'NONE', #7777, #11754, #17324 ) ;
#4364=EDGE_LOOP ( 'NONE', ( #16809, #4302, #2960, #5847, #11879 ) ) ;
#4385=EDGE_CURVE ( 'NONE', #1595, #12357, #7637, .T. ) ;
#4403=LINE ( 'NONE', #9918, #15892 ) ;
#4418=DIRECTION ( 'NONE',  ( -1.000000000000000000, -0.000000000000000000, -0.000000000000000000 ) ) ;
#4451=DIRECTION ( 'NONE',  ( 0.000000000000000000, -1.000000000000000000, 0.000000000000000000 ) ) ;
#4496=VERTEX_POINT ( 'NONE', #11760 ) ;
#4579=ORIENTED_EDGE ( 'NONE', *, *, #14326, .T. ) ;
#4582=EDGE_CURVE ( 'NONE', #11951, #9378, #9200, .T. ) ;
#4590=EDGE_LOOP ( 'NONE', ( #10956, #3188 ) ) ;
#4596=LINE ( 'NONE', #1811, #5006 ) ;
#4631=ORIENTED_EDGE ( 'NONE', *, *, #15161, .F. ) ;
#4637=ORIENTED_EDGE ( 'NONE', *, *, #2514, .F. ) ;
#4641=EDGE_LOOP ( 'NONE', ( #15860, #4130, #7079, #3748 ) ) ;
#4642=DIRECTION ( 'NONE',  ( -1.000000000000000000, -0.000000000000000000, -0.000000000000000000 ) ) ;
#4644=DIRECTION ( 'NONE',  ( -1.000000000000000000, 0.000000000000000000, -0.000000000000000000 ) ) ;
#4685=DIRECTION ( 'NONE',  ( 1.000000000000000000, 0.000000000000000000, 0.000000000000000000 ) ) ;
#4694=EDGE_LOOP ( 'NONE', ( #4150, #4234, #13797 ) ) ;
#4700=TOROIDAL_SURFACE ( 'NONE', #9899, 2.700000000000000622, 0.2000000000000000111 ) ;
#4714=ADVANCED_FACE ( 'NONE', ( #17003 ), #7655, .T. ) ;
#4724=CIRCLE ( 'NONE', #7916, 2.041999999999999815 ) ;
#4741=CARTESIAN_POINT ( 'NONE',  ( 0.000000000000000000, 2.357898499370432166, -2.385244779468109755E-15 ) ) ;
#4767=EDGE_LOOP ( 'NONE', ( #16983, #239, #9851 ) ) ;
#4792=DIRECTION ( 'NONE',  ( 0.000000000000000000, 0.000000000000000000, 1.000000000000000000 ) ) ;
#4802=CARTESIAN_POINT ( 'NONE',  ( 0.000000000000000000, -2.357898499370431722, 2.818925648462311528E-15 ) ) ;
#4808=CARTESIAN_POINT ( 'NONE',  ( 2.500000000000000000, -1.768423874527823125, 1.021000000000002128 ) ) ;
#4819=PRODUCT_DEFINITION_FORMATION_WITH_SPECIFIED_SOURCE ( 'ANY', '', #2317, .NOT_KNOWN. ) ;
#4837=LINE ( 'NONE', #8843, #12132 ) ;
#4861=SURFACE_SIDE_STYLE ('',( #2431 ) ) ;
#4864=AXIS2_PLACEMENT_3D ( 'NONE', #1182, #10671, #8062 ) ;
#4874=ORIENTED_EDGE ( 'NONE', *, *, #15623, .T. ) ;
#4900=CARTESIAN_POINT ( 'NONE',  ( 2.500000000000000000, -2.629050547790028551E-15, -2.041999999999999815 ) ) ;
#4914=EDGE_CURVE ( 'NONE', #17268, #5050, #2552, .T. ) ;
#4945=CARTESIAN_POINT ( 'NONE',  ( 2.500000000000000000, -1.178949249685213863, 2.042000000000001148 ) ) ;
#4959=ORIENTED_EDGE ( 'NONE', *, *, #11848, .T. ) ;
#4966=EDGE_CURVE ( 'NONE', #558, #14684, #1359, .T. ) ;
#4985=CARTESIAN_POINT ( 'NONE',  ( 2.500000000000000000, -2.357898499370431722, 2.818925648462311528E-15 ) ) ;
#5000=DIRECTION ( 'NONE',  ( -0.000000000000000000, 1.103561164596346103E-15, 1.000000000000000000 ) ) ;
#5006=VECTOR ( 'NONE', #14218, 1000.000000000000114 ) ;
#5011=VECTOR ( 'NONE', #7785, 1000.000000000000000 ) ;
#5020=DIRECTION ( 'NONE',  ( -1.000000000000000000, -0.000000000000000000, -0.000000000000000000 ) ) ;
#5043=FILL_AREA_STYLE_COLOUR ( '', #1605 ) ;
#5050=VERTEX_POINT ( 'NONE', #7170 ) ;
#5095=CARTESIAN_POINT ( 'NONE',  ( 0.000000000000000000, 0.000000000000000000, 0.000000000000000000 ) ) ;
#5114=EDGE_LOOP ( 'NONE', ( #17335, #908, #6998, #14930 ) ) ;
#5156=EDGE_CURVE ( 'NONE', #5316, #2160, #12674, .T. ) ;
#5187=CIRCLE ( 'NONE', #12148, 2.041999999999999815 ) ;
#5215=LINE ( 'NONE', #16308, #13101 ) ;
#5223=CARTESIAN_POINT ( 'NONE',  ( 2.500000000000000000, -1.178949249685213863, 2.042000000000001148 ) ) ;
#5235=VECTOR ( 'NONE', #14961, 1000.000000000000114 ) ;
#5260=DIRECTION ( 'NONE',  ( -1.000000000000000000, -0.000000000000000000, -0.000000000000000000 ) ) ;
#5316=VERTEX_POINT ( 'NONE', #15863 ) ;
#5366=( GEOMETRIC_REPRESENTATION_CONTEXT ( 3 ) GLOBAL_UNCERTAINTY_ASSIGNED_CONTEXT ( ( #12292 ) ) GLOBAL_UNIT_ASSIGNED_CONTEXT ( ( #979, #6505, #17522 ) ) REPRESENTATION_CONTEXT ( 'NONE', 'WORKASPACE' ) );
#5440=DIRECTION ( 'NONE',  ( -1.000000000000000000, -0.000000000000000000, -0.000000000000000000 ) ) ;
#5445=VERTEX_POINT ( 'NONE', #2786 ) ;
#5491=DIRECTION ( 'NONE',  ( 0.000000000000000000, 0.000000000000000000, 1.000000000000000000 ) ) ;
#5493=LINE ( 'NONE', #11014, #17451 ) ;
#5530=VECTOR ( 'NONE', #8071, 1000.000000000000000 ) ;
#5550=DIRECTION ( 'NONE',  ( 0.000000000000000000, 0.000000000000000000, 1.000000000000000000 ) ) ;
#5594=AXIS2_PLACEMENT_3D ( 'NONE', #6163, #9789, #14421 ) ;
#5633=ADVANCED_FACE ( 'NONE', ( #15478 ), #17233, .F. ) ;
#5644=ORIENTED_EDGE ( 'NONE', *, *, #6436, .F. ) ;
#5652=CARTESIAN_POINT ( 'NONE',  ( 2.500000000000000000, -1.178949249685213863, 2.042000000000001148 ) ) ;
#5678=ORIENTED_EDGE ( 'NONE', *, *, #7938, .F. ) ;
#5709=DIRECTION ( 'NONE',  ( 0.000000000000000000, -0.5000000000000009992, -0.8660254037844380415 ) ) ;
#5711=ADVANCED_BREP_SHAPE_REPRESENTATION ( '', ( #17325, #3575 ), #5366 ) ;
#5743=PRODUCT_CONTEXT ( 'NONE', #17711, 'mechanical' ) ;
#5745=CARTESIAN_POINT ( 'NONE',  ( 5.200000000000002842, 3.061616997868383634E-16, -2.500000000000000444 ) ) ;
#5803=LINE ( 'NONE', #13985, #6748 ) ;
#5805=ORIENTED_EDGE ( 'NONE', *, *, #5156, .F. ) ;
#5820=CARTESIAN_POINT ( 'NONE',  ( 39.99999999999999289, 0.000000000000000000, 0.000000000000000000 ) ) ;
#5847=ORIENTED_EDGE ( 'NONE', *, *, #9787, .F. ) ;
#5852=SURFACE_STYLE_FILL_AREA ( #345 ) ;
#5913=( GEOMETRIC_REPRESENTATION_CONTEXT ( 3 ) GLOBAL_UNCERTAINTY_ASSIGNED_CONTEXT ( ( #638 ) ) GLOBAL_UNIT_ASSIGNED_CONTEXT ( ( #792, #16216, #7688 ) ) REPRESENTATION_CONTEXT ( 'NONE', 'WORKASPACE' ) );
#5928=LINE ( 'NONE', #7315, #15030 ) ;
#5987=EDGE_CURVE ( 'NONE', #254, #14093, #264, .T. ) ;
#6062=EDGE_CURVE ( 'NONE', #15290, #558, #14354, .T. ) ;
#6091=DIRECTION ( 'NONE',  ( -0.000000000000000000, 0.000000000000000000, 1.000000000000000000 ) ) ;
#6122=ORIENTED_EDGE ( 'NONE', *, *, #16472, .F. ) ;
#6143=ORIENTED_EDGE ( 'NONE', *, *, #15089, .T. ) ;
#6163=CARTESIAN_POINT ( 'NONE',  ( 2.500000000000000000, 0.000000000000000000, 0.000000000000000000 ) ) ;
#6179=ADVANCED_FACE ( 'NONE', ( #7154 ), #8782, .F. ) ;
#6181=AXIS2_PLACEMENT_3D ( 'NONE', #9067, #15870, #4792 ) ;
#6192=DIRECTION ( 'NONE',  ( 0.000000000000000000, 0.000000000000000000, 1.000000000000000000 ) ) ;
#6229=STYLED_ITEM ( 'NONE', ( #9045 ), #5711 ) ;
#6304=AXIS2_PLACEMENT_3D ( 'NONE', #11715, #15812, #6192 ) ;
#6314=LINE ( 'NONE', #10384, #17185 ) ;
#6315=DIRECTION ( 'NONE',  ( -0.000000000000000000, 0.8660254037844391517, 0.4999999999999991673 ) ) ;
#6320=CARTESIAN_POINT ( 'NONE',  ( -31.74999999999995737, 3.061616997868383634E-16, -2.500000000000000444 ) ) ;
#6324=VERTEX_POINT ( 'NONE', #9460 ) ;
#6350=AXIS2_PLACEMENT_3D ( 'NONE', #14400, #16953, #15395 ) ;
#6404=AXIS2_PLACEMENT_3D ( 'NONE', #12619, #199, #11227 ) ;
#6422=EDGE_LOOP ( 'NONE', ( #14409, #6519, #3906, #10325, #6714 ) ) ;
#6429=ORIENTED_EDGE ( 'NONE', *, *, #16598, .F. ) ;
#6436=EDGE_CURVE ( 'NONE', #6324, #2403, #1866, .T. ) ;
#6499=FACE_OUTER_BOUND ( 'NONE', #6422, .T. ) ;
#6505=( NAMED_UNIT ( * ) PLANE_ANGLE_UNIT ( ) SI_UNIT ( $, .RADIAN. ) );
#6508=ORIENTED_EDGE ( 'NONE', *, *, #14965, .F. ) ;
#6519=ORIENTED_EDGE ( 'NONE', *, *, #15803, .F. ) ;
#6596=AXIS2_PLACEMENT_3D ( 'NONE', #11400, #14234, #9759 ) ;
#6604=LINE ( 'NONE', #9159, #15151 ) ;
#6610=ORIENTED_EDGE ( 'NONE', *, *, #4385, .F. ) ;
#6612=AXIS2_PLACEMENT_3D ( 'NONE', #17481, #9099, #14897 ) ;
#6619=CARTESIAN_POINT ( 'NONE',  ( 2.500000000000000000, 1.178949249685213863, -2.042000000000001148 ) ) ;
#6639=EDGE_LOOP ( 'NONE', ( #4637, #568, #3040, #13649, #8111 ) ) ;
#6649=FACE_OUTER_BOUND ( 'NONE', #3453, .T. ) ;
#6703=ORIENTED_EDGE ( 'NONE', *, *, #7938, .T. ) ;
#6705=CONICAL_SURFACE ( 'NONE', #1219, 2.055000000000000160, 0.7853981633974794763 ) ;
#6714=ORIENTED_EDGE ( 'NONE', *, *, #12545, .T. ) ;
#6715=CARTESIAN_POINT ( 'NONE',  ( 0.2500000000000002220, 0.000000000000000000, 0.000000000000000000 ) ) ;
#6737=EDGE_LOOP ( 'NONE', ( #5805, #12459 ) ) ;
#6748=VECTOR ( 'NONE', #5709, 1000.000000000000114 ) ;
#6814=LINE ( 'NONE', #2815, #16843 ) ;
#6851=FACE_OUTER_BOUND ( 'NONE', #10203, .T. ) ;
#6878=AXIS2_PLACEMENT_3D ( 'NONE', #5820, #15534, #5550 ) ;
#6998=ORIENTED_EDGE ( 'NONE', *, *, #9707, .T. ) ;
#6999=CONICAL_SURFACE ( 'NONE', #15401, 2.041999999999999815, 1.047197551196591858 ) ;
#7006=ORIENTED_EDGE ( 'NONE', *, *, #3157, .F. ) ;
#7011=ORIENTED_EDGE ( 'NONE', *, *, #4385, .T. ) ;
#7048=DIRECTION ( 'NONE',  ( 0.000000000000000000, 0.000000000000000000, -1.000000000000000000 ) ) ;
#7058=DIRECTION ( 'NONE',  ( -1.000000000000000000, -0.000000000000000000, -0.000000000000000000 ) ) ;
#7079=ORIENTED_EDGE ( 'NONE', *, *, #17232, .T. ) ;
#7143=LINE ( 'NONE', #3056, #15399 ) ;
#7145=ORIENTED_EDGE ( 'NONE', *, *, #13786, .F. ) ;
#7154=FACE_OUTER_BOUND ( 'NONE', #473, .T. ) ;
#7163=ORIENTED_EDGE ( 'NONE', *, *, #1880, .T. ) ;
#7170=CARTESIAN_POINT ( 'NONE',  ( 5.000000000000002665, 3.306546357697854226E-16, 2.700000000000000622 ) ) ;
#7175=EDGE_CURVE ( 'NONE', #12037, #9975, #5187, .T. ) ;
#7227=ORIENTED_EDGE ( 'NONE', *, *, #9942, .T. ) ;
#7244=CARTESIAN_POINT ( 'NONE',  ( 2.500000000000000000, 0.000000000000000000, 0.000000000000000000 ) ) ;
#7315=CARTESIAN_POINT ( 'NONE',  ( 2.500000000000000000, -2.357898499370431722, 2.818925648462311528E-15 ) ) ;
#7325=EDGE_LOOP ( 'NONE', ( #3031, #16020, #13238, #2024 ) ) ;
#7376=ORIENTED_EDGE ( 'NONE', *, *, #3168, .T. ) ;
#7396=ORIENTED_EDGE ( 'NONE', *, *, #12273, .F. ) ;
#7404=EDGE_CURVE ( 'NONE', #15290, #11575, #2423, .T. ) ;
#7460=ADVANCED_FACE ( 'NONE', ( #7596 ), #13120, .F. ) ;
#7498=ORIENTED_EDGE ( 'NONE', *, *, #1481, .T. ) ;
#7504=PLANE ( 'NONE',  #16605 ) ;
#7511=ADVANCED_FACE ( 'NONE', ( #6499 ), #15841, .T. ) ;
#7547=DIRECTION ( 'NONE',  ( 0.000000000000000000, 0.000000000000000000, -1.000000000000000000 ) ) ;
#7561=AXIS2_PLACEMENT_3D ( 'NONE', #8893, #2011, #11691 ) ;
#7578=ORIENTED_EDGE ( 'NONE', *, *, #8159, .F. ) ;
#7596=FACE_OUTER_BOUND ( 'NONE', #12303, .T. ) ;
#7637=LINE ( 'NONE', #4802, #16445 ) ;
#7655=CYLINDRICAL_SURFACE ( 'NONE', #6304, 2.500000000000000444 ) ;
#7661=DIRECTION ( 'NONE',  ( 0.000000000000000000, -1.000000000000000000, 1.287488025362403787E-15 ) ) ;
#7688=( NAMED_UNIT ( * ) SI_UNIT ( $, .STERADIAN. ) SOLID_ANGLE_UNIT ( ) );
#7741=FACE_OUTER_BOUND ( 'NONE', #4767, .T. ) ;
#7752=DIRECTION ( 'NONE',  ( 1.000000000000000000, 0.000000000000000000, 0.000000000000000000 ) ) ;
#7754=AXIS2_PLACEMENT_3D ( 'NONE', #1944, #4644, #6091 ) ;
#7777=CARTESIAN_POINT ( 'NONE',  ( 5.200000000000002842, 3.306546357697854226E-16, 2.700000000000000622 ) ) ;
#7781=ORIENTED_EDGE ( 'NONE', *, *, #15623, .F. ) ;
#7785=DIRECTION ( 'NONE',  ( -0.7071067811865254793, 0.000000000000000000, 0.7071067811865695552 ) ) ;
#7795=DIRECTION ( 'NONE',  ( 0.000000000000000000, 0.000000000000000000, 1.000000000000000000 ) ) ;
#7837=DIRECTION ( 'NONE',  ( 0.000000000000000000, 0.000000000000000000, 1.000000000000000000 ) ) ;
#7916=AXIS2_PLACEMENT_3D ( 'NONE', #7244, #10025, #8867 ) ;
#7926=PLANE ( 'NONE',  #9028 ) ;
#7935=CARTESIAN_POINT ( 'NONE',  ( 5.000000000000000888, 4.250000000000000000, 0.000000000000000000 ) ) ;
#7938=EDGE_CURVE ( 'NONE', #16655, #12357, #14464, .T. ) ;
#7975=DIRECTION ( 'NONE',  ( 0.000000000000000000, -0.4999999999999992228, 0.8660254037844390407 ) ) ;
#8015=AXIS2_PLACEMENT_3D ( 'NONE', #2488, #13469, #13549 ) ;
#8027=CIRCLE ( 'NONE', #216, 0.2000000000000000944 ) ;
#8062=DIRECTION ( 'NONE',  ( 0.000000000000000000, 0.000000000000000000, -1.000000000000000000 ) ) ;
#8071=DIRECTION ( 'NONE',  ( -1.000000000000000000, -0.000000000000000000, -0.000000000000000000 ) ) ;
#8073=DIRECTION ( 'NONE',  ( -1.000000000000000000, -0.000000000000000000, -0.000000000000000000 ) ) ;
#8111=ORIENTED_EDGE ( 'NONE', *, *, #9068, .T. ) ;
#8159=EDGE_CURVE ( 'NONE', #2513, #10545, #17701, .T. ) ;
#8241=ORIENTED_EDGE ( 'NONE', *, *, #1824, .F. ) ;
#8341=AXIS2_PLACEMENT_3D ( 'NONE', #7935, #7752, #2330 ) ;
#8387=LINE ( 'NONE', #15467, #653 ) ;
#8399=DIRECTION ( 'NONE',  ( 0.000000000000000000, 0.000000000000000000, 1.000000000000000000 ) ) ;
#8416=EDGE_LOOP ( 'NONE', ( #9081, #9699, #2724, #6143 ) ) ;
#8465=AXIS2_PLACEMENT_3D ( 'NONE', #3356, #10314, #7795 ) ;
#8467=ORIENTED_EDGE ( 'NONE', *, *, #11942, .F. ) ;
#8510=ORIENTED_EDGE ( 'NONE', *, *, #5987, .T. ) ;
#8636=CARTESIAN_POINT ( 'NONE',  ( -31.74999999999995737, 0.000000000000000000, 0.000000000000000000 ) ) ;
#8648=ADVANCED_FACE ( 'NONE', ( #13297 ), #7504, .T. ) ;
#8653=FACE_OUTER_BOUND ( 'NONE', #11462, .T. ) ;
#8677=DIRECTION ( 'NONE',  ( -1.000000000000000000, -0.000000000000000000, -0.000000000000000000 ) ) ;
#8684=FACE_OUTER_BOUND ( 'NONE', #3212, .T. ) ;
#8727=LINE ( 'NONE', #16987, #3489 ) ;
#8737=PLANE ( 'NONE',  #7754 ) ;
#8752=DIRECTION ( 'NONE',  ( 0.000000000000000000, 0.000000000000000000, -1.000000000000000000 ) ) ;
#8782=PLANE ( 'NONE',  #10667 ) ;
#8784=AXIS2_PLACEMENT_3D ( 'NONE', #10539, #9276, #7837 ) ;
#8786=ORIENTED_EDGE ( 'NONE', *, *, #14794, .T. ) ;
#8806=VERTEX_POINT ( 'NONE', #280 ) ;
#8809=FACE_OUTER_BOUND ( 'NONE', #4590, .T. ) ;
#8819=DIRECTION ( 'NONE',  ( 1.000000000000000000, 0.000000000000000000, 0.000000000000000000 ) ) ;
#8839=DIRECTION ( 'NONE',  ( -0.7071067811865254793, 8.659560562355202797E-17, -0.7071067811865695552 ) ) ;
#8843=CARTESIAN_POINT ( 'NONE',  ( 2.500000000000000000, 1.178949249685218081, 2.041999999999998483 ) ) ;
#8844=EDGE_CURVE ( 'NONE', #15290, #6324, #6604, .T. ) ;
#8846=CARTESIAN_POINT ( 'NONE',  ( 39.55500000000002103, 3.061616997868384127E-16, -2.500000000000000888 ) ) ;
#8867=DIRECTION ( 'NONE',  ( 0.000000000000000000, 0.000000000000000000, 1.000000000000000000 ) ) ;
#8893=CARTESIAN_POINT ( 'NONE',  ( 40.00000000000000000, 2.055000000000000160, 0.000000000000000000 ) ) ;
#8894=ORIENTED_EDGE ( 'NONE', *, *, #3157, .T. ) ;
#8947=DIRECTION ( 'NONE',  ( 0.000000000000000000, 0.5000000000000009992, 0.8660254037844380415 ) ) ;
#8952=CARTESIAN_POINT ( 'NONE',  ( 2.500000000000000000, 1.178949249685213863, -2.042000000000001148 ) ) ;
#9028=AXIS2_PLACEMENT_3D ( 'NONE', #10018, #13185, #9105 ) ;
#9039=CARTESIAN_POINT ( 'NONE',  ( 2.500000000000000000, 2.357898499370432166, -2.385244779468109755E-15 ) ) ;
#9045=PRESENTATION_STYLE_ASSIGNMENT (( #10390 ) ) ;
#9067=CARTESIAN_POINT ( 'NONE',  ( 2.500000000000000000, 0.000000000000000000, 0.000000000000000000 ) ) ;
#9068=EDGE_CURVE ( 'NONE', #2513, #15456, #4724, .T. ) ;
#9077=EDGE_CURVE ( 'NONE', #4496, #12037, #4596, .T. ) ;
#9081=ORIENTED_EDGE ( 'NONE', *, *, #1252, .F. ) ;
#9099=DIRECTION ( 'NONE',  ( -1.000000000000000000, -0.000000000000000000, -0.000000000000000000 ) ) ;
#9105=DIRECTION ( 'NONE',  ( 0.000000000000000000, 0.000000000000000000, -1.000000000000000000 ) ) ;
#9120=EDGE_CURVE ( 'NONE', #1819, #16114, #17675, .T. ) ;
#9134=MECHANICAL_DESIGN_GEOMETRIC_PRESENTATION_REPRESENTATION('',(#6229),#5913);
#9159=CARTESIAN_POINT ( 'NONE',  ( 2.500000000000000000, 2.357898499370432166, -2.385244779468109755E-15 ) ) ;
#9188=TOROIDAL_SURFACE ( 'NONE', #8015, 4.000000000000000000, 0.2500000000000000000 ) ;
#9200=CIRCLE ( 'NONE', #6878, 2.055000000000000160 ) ;
#9272=DIRECTION ( 'NONE',  ( 1.000000000000000000, 0.000000000000000000, 0.000000000000000000 ) ) ;
#9276=DIRECTION ( 'NONE',  ( -1.000000000000000000, -0.000000000000000000, -0.000000000000000000 ) ) ;
#9286=FACE_OUTER_BOUND ( 'NONE', #6737, .T. ) ;
#9295=CIRCLE ( 'NONE', #6404, 0.2500000000000002220 ) ;
#9303=EDGE_CURVE ( 'NONE', #15953, #15303, #15043, .T. ) ;
#9332=FACE_OUTER_BOUND ( 'NONE', #3099, .T. ) ;
#9343=UNCERTAINTY_MEASURE_WITH_UNIT (LENGTH_MEASURE( 1.000000000000000082E-05 ), #3239, 'distance_accuracy_value', 'NONE');
#9348=DIRECTION ( 'NONE',  ( 1.000000000000000000, 0.000000000000000000, 0.000000000000000000 ) ) ;
#9378=VERTEX_POINT ( 'NONE', #16044 ) ;
#9380=EDGE_CURVE ( 'NONE', #15303, #13014, #791, .T. ) ;
#9425=CARTESIAN_POINT ( 'NONE',  ( 0.000000000000000000, 0.000000000000000000, 4.000000000000000000 ) ) ;
#9460=CARTESIAN_POINT ( 'NONE',  ( 2.500000000000000000, 1.768423874527822903, -1.021000000000002350 ) ) ;
#9472=PLANE ( 'NONE',  #11938 ) ;
#9501=CIRCLE ( 'NONE', #3135, 2.500000000000000444 ) ;
#9528=VECTOR ( 'NONE', #15346, 1000.000000000000000 ) ;
#9599=VECTOR ( 'NONE', #7661, 1000.000000000000000 ) ;
#9611=ADVANCED_FACE ( 'NONE', ( #14190 ), #1507, .F. ) ;
#9682=LINE ( 'NONE', #12334, #2949 ) ;
#9699=ORIENTED_EDGE ( 'NONE', *, *, #14498, .T. ) ;
#9707=EDGE_CURVE ( 'NONE', #13014, #8806, #594, .T. ) ;
#9708=EDGE_LOOP ( 'NONE', ( #15937, #11850 ) ) ;
#9759=DIRECTION ( 'NONE',  ( 0.000000000000000000, 0.000000000000000000, 1.000000000000000000 ) ) ;
#9787=EDGE_CURVE ( 'NONE', #5445, #15456, #15740, .T. ) ;
#9789=DIRECTION ( 'NONE',  ( -1.000000000000000000, -0.000000000000000000, -0.000000000000000000 ) ) ;
#9795=LINE ( 'NONE', #16534, #9528 ) ;
#9851=ORIENTED_EDGE ( 'NONE', *, *, #12669, .F. ) ;
#9866=ORIENTED_EDGE ( 'NONE', *, *, #8844, .F. ) ;
#9899=AXIS2_PLACEMENT_3D ( 'NONE', #1955, #15732, #8752 ) ;
#9918=CARTESIAN_POINT ( 'NONE',  ( -31.74999999999995737, 0.000000000000000000, 2.500000000000000444 ) ) ;
#9942=EDGE_CURVE ( 'NONE', #15303, #15953, #1766, .T. ) ;
#9947=ORIENTED_EDGE ( 'NONE', *, *, #5156, .T. ) ;
#9975=VERTEX_POINT ( 'NONE', #12081 ) ;
#9980=CARTESIAN_POINT ( 'NONE',  ( 39.99999999999999289, 0.000000000000000000, 0.000000000000000000 ) ) ;
#10016=SURFACE_STYLE_USAGE ( .BOTH. , #11375 ) ;
#10018=CARTESIAN_POINT ( 'NONE',  ( 2.500000000000000000, 2.357898499370432166, -2.385244779468109755E-15 ) ) ;
#10025=DIRECTION ( 'NONE',  ( -1.000000000000000000, -0.000000000000000000, -0.000000000000000000 ) ) ;
#10059=ORIENTED_EDGE ( 'NONE', *, *, #16598, .T. ) ;
#10082=ORIENTED_EDGE ( 'NONE', *, *, #9707, .F. ) ;
#10100=ADVANCED_FACE ( 'NONE', ( #8809 ), #15786, .T. ) ;
#10111=FACE_OUTER_BOUND ( 'NONE', #7325, .T. ) ;
#10112=AXIS2_PLACEMENT_3D ( 'NONE', #12642, #328, #232 ) ;
#10196=VECTOR ( 'NONE', #10744, 1000.000000000000114 ) ;
#10203=EDGE_LOOP ( 'NONE', ( #2158, #13496, #16171, #395, #14568 ) ) ;
#10293=DIRECTION ( 'NONE',  ( 0.000000000000000000, 0.000000000000000000, 1.000000000000000000 ) ) ;
#10301=ORIENTED_EDGE ( 'NONE', *, *, #7175, .F. ) ;
#10314=DIRECTION ( 'NONE',  ( -1.000000000000000000, -0.000000000000000000, -0.000000000000000000 ) ) ;
#10325=ORIENTED_EDGE ( 'NONE', *, *, #8159, .T. ) ;
#10331=CARTESIAN_POINT ( 'NONE',  ( -31.74999999999995737, 0.000000000000000000, 0.000000000000000000 ) ) ;
#10347=EDGE_CURVE ( 'NONE', #8806, #5050, #12179, .T. ) ;
#10348=ADVANCED_FACE ( 'NONE', ( #10394 ), #11001, .F. ) ;
#10381=AXIS2_PLACEMENT_3D ( 'NONE', #6715, #9348, #17737 ) ;
#10384=CARTESIAN_POINT ( 'NONE',  ( 2.500000000000000000, -1.178949249685213863, 2.042000000000001148 ) ) ;
#10390=SURFACE_STYLE_USAGE ( .BOTH. , #4861 ) ;
#10394=FACE_OUTER_BOUND ( 'NONE', #1764, .T. ) ;
#10474=DIRECTION ( 'NONE',  ( 0.000000000000000000, 0.8660254037844380415, -0.5000000000000009992 ) ) ;
#10475=DIRECTION ( 'NONE',  ( -1.000000000000000000, -0.000000000000000000, -0.000000000000000000 ) ) ;
#10519=FACE_OUTER_BOUND ( 'NONE', #4694, .T. ) ;
#10532=EDGE_LOOP ( 'NONE', ( #6610, #17536, #4579, #171, #15264 ) ) ;
#10539=CARTESIAN_POINT ( 'NONE',  ( 0.000000000000000000, 0.000000000000000000, 0.000000000000000000 ) ) ;
#10545=VERTEX_POINT ( 'NONE', #4985 ) ;
#10572=VERTEX_POINT ( 'NONE', #16074 ) ;
#10667=AXIS2_PLACEMENT_3D ( 'NONE', #12939, #4685, #11472 ) ;
#10671=DIRECTION ( 'NONE',  ( 1.000000000000000000, 0.000000000000000000, 0.000000000000000000 ) ) ;
#10737=CIRCLE ( 'NONE', #13081, 0.2500000000000002220 ) ;
#10744=DIRECTION ( 'NONE',  ( 0.000000000000000000, -0.5000000000000009992, -0.8660254037844380415 ) ) ;
#10773=DIRECTION ( 'NONE',  ( 0.000000000000000000, -1.000000000000000000, 1.287488025362403787E-15 ) ) ;
#10883=CARTESIAN_POINT ( 'NONE',  ( 0.2500000000000002220, 0.000000000000000000, 4.250000000000000000 ) ) ;
#10916=ADVANCED_FACE ( 'NONE', ( #17087 ), #3107, .T. ) ;
#10954=DIRECTION ( 'NONE',  ( 0.000000000000000000, 0.000000000000000000, -1.000000000000000000 ) ) ;
#10956=ORIENTED_EDGE ( 'NONE', *, *, #4582, .F. ) ;
#10967=AXIS2_PLACEMENT_3D ( 'NONE', #14720, #5260, #12063 ) ;
#10969=ADVANCED_FACE ( 'NONE', ( #12154 ), #748, .F. ) ;
#10983=ORIENTED_EDGE ( 'NONE', *, *, #9120, .F. ) ;
#11001=PLANE ( 'NONE',  #14503 ) ;
#11014=CARTESIAN_POINT ( 'NONE',  ( -31.74999999999995737, 5.204748896376250699E-16, -4.250000000000000000 ) ) ;
#11026=AXIS2_PLACEMENT_3D ( 'NONE', #3414, #4418, #12934 ) ;
#11033=CARTESIAN_POINT ( 'NONE',  ( 2.500000000000000000, 2.357898499370432166, -2.385244779468109755E-15 ) ) ;
#11121=EDGE_CURVE ( 'NONE', #254, #16114, #10737, .T. ) ;
#11160=CARTESIAN_POINT ( 'NONE',  ( 39.55500000000002103, 0.000000000000000000, 2.500000000000000888 ) ) ;
#11162=EDGE_CURVE ( 'NONE', #15456, #14684, #6814, .T. ) ;
#11164=DIRECTION ( 'NONE',  ( 0.000000000000000000, 1.000000000000000000, -1.103561164596346103E-15 ) ) ;
#11227=DIRECTION ( 'NONE',  ( 0.000000000000000000, 0.000000000000000000, -1.000000000000000000 ) ) ;
#11242=VECTOR ( 'NONE', #11841, 1000.000000000000000 ) ;
#11261=EDGE_CURVE ( 'NONE', #5316, #14093, #7143, .T. ) ;
#11288=AXIS2_PLACEMENT_3D ( 'NONE', #8636, #4642, #14166 ) ;
#11324=CIRCLE ( 'NONE', #5594, 2.041999999999999815 ) ;
#11348=CARTESIAN_POINT ( 'NONE',  ( 2.500000000000000000, 2.357898499370432166, -2.385244779468109755E-15 ) ) ;
#11365=STYLED_ITEM ( 'NONE', ( #17954 ), #17325 ) ;
#11375=SURFACE_SIDE_STYLE ('',( #5852 ) ) ;
#11400=CARTESIAN_POINT ( 'NONE',  ( 5.000000000000004441, 0.000000000000000000, 0.000000000000000000 ) ) ;
#11462=EDGE_LOOP ( 'NONE', ( #7006, #15129, #13313, #15885 ) ) ;
#11472=DIRECTION ( 'NONE',  ( 0.000000000000000000, 0.000000000000000000, -1.000000000000000000 ) ) ;
#11545=CARTESIAN_POINT ( 'NONE',  ( 2.500000000000000000, 2.253471898105738645E-15, 2.041999999999999815 ) ) ;
#11575=VERTEX_POINT ( 'NONE', #4741 ) ;
#11612=DIRECTION ( 'NONE',  ( -1.000000000000000000, -0.000000000000000000, -0.000000000000000000 ) ) ;
#11649=APPLICATION_CONTEXT ( 'automotive_design' ) ;
#11691=DIRECTION ( 'NONE',  ( 0.000000000000000000, 0.000000000000000000, -1.000000000000000000 ) ) ;
#11715=CARTESIAN_POINT ( 'NONE',  ( -31.74999999999995737, 0.000000000000000000, 0.000000000000000000 ) ) ;
#11743=( NAMED_UNIT ( * ) PLANE_ANGLE_UNIT ( ) SI_UNIT ( $, .RADIAN. ) );
#11744=DIRECTION ( 'NONE',  ( 1.000000000000000000, 0.000000000000000000, 0.000000000000000000 ) ) ;
#11746=DIRECTION ( 'NONE',  ( 0.000000000000000000, 0.000000000000000000, 1.000000000000000000 ) ) ;
#11754=DIRECTION ( 'NONE',  ( 0.000000000000000000, 1.000000000000000000, -1.224646799147353207E-16 ) ) ;
#11760=CARTESIAN_POINT ( 'NONE',  ( 3.678949249685231848, 0.000000000000000000, 0.000000000000000000 ) ) ;
#11832=( NAMED_UNIT ( * ) SI_UNIT ( $, .STERADIAN. ) SOLID_ANGLE_UNIT ( ) );
#11841=DIRECTION ( 'NONE',  ( -1.000000000000000000, -0.000000000000000000, -0.000000000000000000 ) ) ;
#11848=EDGE_CURVE ( 'NONE', #11575, #12285, #8727, .T. ) ;
#11850=ORIENTED_EDGE ( 'NONE', *, *, #1009, .T. ) ;
#11879=ORIENTED_EDGE ( 'NONE', *, *, #15803, .T. ) ;
#11916=CONICAL_SURFACE ( 'NONE', #4110, 2.041999999999999815, 1.047197551196591858 ) ;
#11938=AXIS2_PLACEMENT_3D ( 'NONE', #12378, #13659, #1248 ) ;
#11942=EDGE_CURVE ( 'NONE', #14093, #1819, #9295, .T. ) ;
#11951=VERTEX_POINT ( 'NONE', #17080 ) ;
#11973=CARTESIAN_POINT ( 'NONE',  ( 0.000000000000000000, 1.178949249685218081, 2.041999999999998483 ) ) ;
#11974=CARTESIAN_POINT ( 'NONE',  ( 2.500000000000000000, 0.000000000000000000, 2.041999999999999815 ) ) ;
#11987=ORIENTED_EDGE ( 'NONE', *, *, #14965, .T. ) ;
#12015=ADVANCED_FACE ( 'NONE', ( #2293 ), #16079, .T. ) ;
#12037=VERTEX_POINT ( 'NONE', #4900 ) ;
#12053=CARTESIAN_POINT ( 'NONE',  ( 0.000000000000000000, -1.178949249685213863, 2.042000000000001148 ) ) ;
#12063=DIRECTION ( 'NONE',  ( 0.000000000000000000, 0.000000000000000000, 1.000000000000000000 ) ) ;
#12069=ORIENTED_EDGE ( 'NONE', *, *, #16213, .T. ) ;
#12081=CARTESIAN_POINT ( 'NONE',  ( 2.500000000000000000, -1.768423874527824902, -1.020999999999998353 ) ) ;
#12090=ADVANCED_FACE ( 'NONE', ( #10519 ), #2022, .F. ) ;
#12097=TOROIDAL_SURFACE ( 'NONE', #4864, 2.700000000000000622, 0.2000000000000000111 ) ;
#12132=VECTOR ( 'NONE', #13192, 1000.000000000000000 ) ;
#12133=CARTESIAN_POINT ( 'NONE',  ( 0.000000000000000000, 1.178949249685213863, -2.042000000000001148 ) ) ;
#12148=AXIS2_PLACEMENT_3D ( 'NONE', #15292, #7058, #8399 ) ;
#12154=FACE_OUTER_BOUND ( 'NONE', #4364, .T. ) ;
#12179=CIRCLE ( 'NONE', #4354, 0.2000000000000000944 ) ;
#12230=EDGE_CURVE ( 'NONE', #10572, #1595, #2638, .T. ) ;
#12272=ORIENTED_EDGE ( 'NONE', *, *, #11121, .T. ) ;
#12273=EDGE_CURVE ( 'NONE', #2403, #16655, #14880, .T. ) ;
#12285=VERTEX_POINT ( 'NONE', #11973 ) ;
#12292=UNCERTAINTY_MEASURE_WITH_UNIT (LENGTH_MEASURE( 1.000000000000000082E-05 ), #979, 'distance_accuracy_value', 'NONE');
#12303=EDGE_LOOP ( 'NONE', ( #13041, #2865, #6429 ) ) ;
#12333=FACE_OUTER_BOUND ( 'NONE', #8416, .T. ) ;
#12334=CARTESIAN_POINT ( 'NONE',  ( 2.500000000000000000, 1.178949249685213863, -2.042000000000001148 ) ) ;
#12357=VERTEX_POINT ( 'NONE', #272 ) ;
#12378=CARTESIAN_POINT ( 'NONE',  ( 2.500000000000000000, 2.357898499370432166, -2.385244779468109755E-15 ) ) ;
#12388=ORIENTED_EDGE ( 'NONE', *, *, #4966, .F. ) ;
#12459=ORIENTED_EDGE ( 'NONE', *, *, #14498, .F. ) ;
#12519=DIRECTION ( 'NONE',  ( 0.000000000000000000, -1.224646799147353454E-16, 1.000000000000000000 ) ) ;
#12545=EDGE_CURVE ( 'NONE', #10545, #1595, #3706, .T. ) ;
#12557=DIRECTION ( 'NONE',  ( 1.000000000000000000, 0.000000000000000000, 0.000000000000000000 ) ) ;
#12610=CARTESIAN_POINT ( 'NONE',  ( 2.500000000000000000, 1.178949249685218081, 2.041999999999998483 ) ) ;
#12619=CARTESIAN_POINT ( 'NONE',  ( 0.2500000000000002220, 0.000000000000000000, 4.000000000000000000 ) ) ;
#12642=CARTESIAN_POINT ( 'NONE',  ( 2.500000000000000000, 2.357898499370432166, -2.385244779468109755E-15 ) ) ;
#12669=EDGE_CURVE ( 'NONE', #558, #6324, #17752, .T. ) ;
#12674=CIRCLE ( 'NONE', #6596, 4.250000000000000000 ) ;
#12686=CARTESIAN_POINT ( 'NONE',  ( 2.500000000000000000, 2.357898499370432166, -2.385244779468109755E-15 ) ) ;
#12724=EDGE_LOOP ( 'NONE', ( #7163, #7145, #10301 ) ) ;
#12738=DIRECTION ( 'NONE',  ( -1.000000000000000000, -0.000000000000000000, -0.000000000000000000 ) ) ;
#12748=FILL_AREA_STYLE_COLOUR ( '', #3581 ) ;
#12780=DIRECTION ( 'NONE',  ( 0.000000000000000000, 0.000000000000000000, -1.000000000000000000 ) ) ;
#12800=ADVANCED_FACE ( 'NONE', ( #3583 ), #6705, .T. ) ;
#12853=DIRECTION ( 'NONE',  ( -1.000000000000000000, -0.000000000000000000, -0.000000000000000000 ) ) ;
#12893=ADVANCED_FACE ( 'NONE', ( #7741 ), #7926, .F. ) ;
#12934=DIRECTION ( 'NONE',  ( 0.000000000000000000, 0.000000000000000000, 1.000000000000000000 ) ) ;
#12939=CARTESIAN_POINT ( 'NONE',  ( 2.500000000000000000, 2.357898499370432166, -2.385244779468109755E-15 ) ) ;
#12962=PRODUCT_DEFINITION_CONTEXT ( 'detailed design', #11649, 'design' ) ;
#13014=VERTEX_POINT ( 'NONE', #5745 ) ;
#13039=VECTOR ( 'NONE', #11164, 1000.000000000000000 ) ;
#13041=ORIENTED_EDGE ( 'NONE', *, *, #6436, .T. ) ;
#13052=ADVANCED_FACE ( 'NONE', ( #2559 ), #11916, .F. ) ;
#13053=CARTESIAN_POINT ( 'NONE',  ( 5.000000000000004441, 5.204748896376250699E-16, -4.250000000000000000 ) ) ;
#13081=AXIS2_PLACEMENT_3D ( 'NONE', #1558, #13874, #12519 ) ;
#13101=VECTOR ( 'NONE', #15104, 1000.000000000000114 ) ;
#13120=PLANE ( 'NONE',  #17104 ) ;
#13126=DIRECTION ( 'NONE',  ( 0.000000000000000000, -1.287488025362403787E-15, -1.000000000000000000 ) ) ;
#13185=DIRECTION ( 'NONE',  ( 1.000000000000000000, 0.000000000000000000, 0.000000000000000000 ) ) ;
#13192=DIRECTION ( 'NONE',  ( -1.000000000000000000, -0.000000000000000000, -0.000000000000000000 ) ) ;
#13238=ORIENTED_EDGE ( 'NONE', *, *, #11942, .T. ) ;
#13263=DIRECTION ( 'NONE',  ( 0.000000000000000000, -0.4999999999999992228, 0.8660254037844390407 ) ) ;
#13297=FACE_OUTER_BOUND ( 'NONE', #10532, .T. ) ;
#13313=ORIENTED_EDGE ( 'NONE', *, *, #4914, .F. ) ;
#13317=CARTESIAN_POINT ( 'NONE',  ( 5.000000000000002665, 0.000000000000000000, -2.700000000000000622 ) ) ;
#13320=CARTESIAN_POINT ( 'NONE',  ( 2.500000000000000000, -2.357898499370431722, 2.818925648462311528E-15 ) ) ;
#13380=VECTOR ( 'NONE', #16059, 1000.000000000000000 ) ;
#13434=DIRECTION ( 'NONE',  ( 0.000000000000000000, 0.4999999999999991118, -0.8660254037844391517 ) ) ;
#13444=DIRECTION ( 'NONE',  ( 0.000000000000000000, -1.000000000000000000, 1.103561164596346103E-15 ) ) ;
#13469=DIRECTION ( 'NONE',  ( -1.000000000000000000, -0.000000000000000000, -0.000000000000000000 ) ) ;
#13480=ORIENTED_EDGE ( 'NONE', *, *, #1252, .T. ) ;
#13494=ADVANCED_FACE ( 'NONE', ( #9332 ), #12097, .F. ) ;
#13496=ORIENTED_EDGE ( 'NONE', *, *, #7404, .F. ) ;
#13549=DIRECTION ( 'NONE',  ( 0.000000000000000000, 0.000000000000000000, 1.000000000000000000 ) ) ;
#13592=CARTESIAN_POINT ( 'NONE',  ( 2.500000000000000000, 1.178949249685213863, -2.042000000000001148 ) ) ;
#13649=ORIENTED_EDGE ( 'NONE', *, *, #16607, .T. ) ;
#13659=DIRECTION ( 'NONE',  ( 0.000000000000000000, -0.8660254037844390407, -0.4999999999999992784 ) ) ;
#13751=DIRECTION ( 'NONE',  ( 0.000000000000000000, 0.8660254037844380415, -0.5000000000000011102 ) ) ;
#13786=EDGE_CURVE ( 'NONE', #9975, #17674, #5928, .T. ) ;
#13797=ORIENTED_EDGE ( 'NONE', *, *, #9068, .F. ) ;
#13874=DIRECTION ( 'NONE',  ( -0.000000000000000000, 1.000000000000000000, 1.224646799147353207E-16 ) ) ;
#13948=VECTOR ( 'NONE', #1285, 1000.000000000000000 ) ;
#13966=FACE_OUTER_BOUND ( 'NONE', #12724, .T. ) ;
#13985=CARTESIAN_POINT ( 'NONE',  ( 2.500000000000000000, -1.178949249685213863, 2.042000000000001148 ) ) ;
#13999=EDGE_CURVE ( 'NONE', #14684, #12285, #4837, .T. ) ;
#14011=ORIENTED_EDGE ( 'NONE', *, *, #12273, .T. ) ;
#14020=CARTESIAN_POINT ( 'NONE',  ( 0.2500000000000002220, 0.000000000000000000, 0.000000000000000000 ) ) ;
#14093=VERTEX_POINT ( 'NONE', #10883 ) ;
#14142=DIRECTION ( 'NONE',  ( 1.000000000000000000, 0.000000000000000000, 0.000000000000000000 ) ) ;
#14166=DIRECTION ( 'NONE',  ( 0.000000000000000000, 0.000000000000000000, 1.000000000000000000 ) ) ;
#14174=EDGE_CURVE ( 'NONE', #9378, #11951, #15044, .T. ) ;
#14190=FACE_OUTER_BOUND ( 'NONE', #14273, .T. ) ;
#14218=DIRECTION ( 'NONE',  ( -0.5000000000000051070, 1.060575238724903217E-16, -0.8660254037844355990 ) ) ;
#14233=LINE ( 'NONE', #1821, #5011 ) ;
#14234=DIRECTION ( 'NONE',  ( -1.000000000000000000, -0.000000000000000000, -0.000000000000000000 ) ) ;
#14244=TOROIDAL_SURFACE ( 'NONE', #1223, 4.000000000000000000, 0.2500000000000000000 ) ;
#14245=AXIS2_PLACEMENT_3D ( 'NONE', #12686, #14142, #12780 ) ;
#14273=EDGE_LOOP ( 'NONE', ( #1719, #7578, #3140 ) ) ;
#14326=EDGE_CURVE ( 'NONE', #10545, #9975, #9795, .T. ) ;
#14353=CARTESIAN_POINT ( 'NONE',  ( 0.000000000000000000, -2.357898499370431722, 2.818925648462311528E-15 ) ) ;
#14354=LINE ( 'NONE', #1940, #3448 ) ;
#14400=CARTESIAN_POINT ( 'NONE',  ( 0.000000000000000000, 0.000000000000000000, 0.000000000000000000 ) ) ;
#14409=ORIENTED_EDGE ( 'NONE', *, *, #12230, .F. ) ;
#14421=DIRECTION ( 'NONE',  ( 0.000000000000000000, 0.000000000000000000, 1.000000000000000000 ) ) ;
#14464=LINE ( 'NONE', #15817, #9599 ) ;
#14478=AXIS2_PLACEMENT_3D ( 'NONE', #9980, #16715, #1758 ) ;
#14498=EDGE_CURVE ( 'NONE', #2160, #5316, #865, .T. ) ;
#14503=AXIS2_PLACEMENT_3D ( 'NONE', #16394, #13751, #2511 ) ;
#14517=AXIS2_PLACEMENT_3D ( 'NONE', #741, #8819, #7547 ) ;
#14568=ORIENTED_EDGE ( 'NONE', *, *, #13999, .T. ) ;
#14669=CARTESIAN_POINT ( 'NONE',  ( 2.500000000000000000, 2.357898499370432166, -2.385244779468109755E-15 ) ) ;
#14684=VERTEX_POINT ( 'NONE', #12610 ) ;
#14695=FACE_OUTER_BOUND ( 'NONE', #4641, .T. ) ;
#14720=CARTESIAN_POINT ( 'NONE',  ( 5.000000000000004441, 0.000000000000000000, 0.000000000000000000 ) ) ;
#14794=EDGE_CURVE ( 'NONE', #13014, #17268, #8027, .T. ) ;
#14805=CARTESIAN_POINT ( 'NONE',  ( 2.500000000000000000, -1.178949249685213863, 2.042000000000001148 ) ) ;
#14835=ORIENTED_EDGE ( 'NONE', *, *, #12230, .T. ) ;
#14880=LINE ( 'NONE', #6619, #5530 ) ;
#14897=DIRECTION ( 'NONE',  ( 0.000000000000000000, 0.000000000000000000, -1.000000000000000000 ) ) ;
#14930=ORIENTED_EDGE ( 'NONE', *, *, #3168, .F. ) ;
#14961=DIRECTION ( 'NONE',  ( 0.000000000000000000, -0.5000000000000009992, -0.8660254037844380415 ) ) ;
#14965=EDGE_CURVE ( 'NONE', #11575, #16655, #5215, .T. ) ;
#14984=CARTESIAN_POINT ( 'NONE',  ( 2.500000000000000000, 1.178949249685213863, -2.042000000000001148 ) ) ;
#15030=VECTOR ( 'NONE', #4309, 1000.000000000000000 ) ;
#15043=CIRCLE ( 'NONE', #2028, 2.500000000000000888 ) ;
#15044=CIRCLE ( 'NONE', #14478, 2.055000000000000160 ) ;
#15060=ADVANCED_FACE ( 'NONE', ( #6851 ), #9472, .T. ) ;
#15071=EDGE_LOOP ( 'NONE', ( #16563, #7498, #17357, #1117 ) ) ;
#15081=AXIS2_PLACEMENT_3D ( 'NONE', #10331, #11612, #17365 ) ;
#15089=EDGE_CURVE ( 'NONE', #14093, #254, #16585, .T. ) ;
#15104=DIRECTION ( 'NONE',  ( 0.000000000000000000, -0.5000000000000011102, -0.8660254037844379305 ) ) ;
#15129=ORIENTED_EDGE ( 'NONE', *, *, #10347, .T. ) ;
#15151=VECTOR ( 'NONE', #2102, 1000.000000000000114 ) ;
#15153=ORIENTED_EDGE ( 'NONE', *, *, #7404, .T. ) ;
#15161=EDGE_CURVE ( 'NONE', #10572, #12285, #8387, .T. ) ;
#15165=CIRCLE ( 'NONE', #6181, 2.041999999999999815 ) ;
#15193=PRODUCT_DEFINITION_SHAPE ( 'NONE', 'NONE',  #817 ) ;
#15202=ORIENTED_EDGE ( 'NONE', *, *, #1880, .F. ) ;
#15264=ORIENTED_EDGE ( 'NONE', *, *, #1824, .T. ) ;
#15290=VERTEX_POINT ( 'NONE', #3673 ) ;
#15292=CARTESIAN_POINT ( 'NONE',  ( 2.500000000000000000, 0.000000000000000000, 0.000000000000000000 ) ) ;
#15303=VERTEX_POINT ( 'NONE', #8846 ) ;
#15343=AXIS2_PLACEMENT_3D ( 'NONE', #4945, #10474, #8947 ) ;
#15346=DIRECTION ( 'NONE',  ( 0.000000000000000000, 0.4999999999999991118, -0.8660254037844391517 ) ) ;
#15395=DIRECTION ( 'NONE',  ( 0.000000000000000000, 0.000000000000000000, 1.000000000000000000 ) ) ;
#15399=VECTOR ( 'NONE', #8677, 1000.000000000000000 ) ;
#15401=AXIS2_PLACEMENT_3D ( 'NONE', #1806, #12853, #11746 ) ;
#15405=EDGE_LOOP ( 'NONE', ( #16223, #12069 ) ) ;
#15456=VERTEX_POINT ( 'NONE', #11545 ) ;
#15467=CARTESIAN_POINT ( 'NONE',  ( 0.000000000000000000, -1.178949249685213863, 2.042000000000001148 ) ) ;
#15478=FACE_OUTER_BOUND ( 'NONE', #2875, .T. ) ;
#15521=DIRECTION ( 'NONE',  ( 0.000000000000000000, -0.4999999999999992228, 0.8660254037844390407 ) ) ;
#15534=DIRECTION ( 'NONE',  ( -1.000000000000000000, -0.000000000000000000, -0.000000000000000000 ) ) ;
#15541=CARTESIAN_POINT ( 'NONE',  ( 0.000000000000000000, 5.051668046482832750E-16, -4.000000000000000000 ) ) ;
#15551=DIRECTION ( 'NONE',  ( 0.000000000000000000, 1.000000000000000000, -1.103561164596346103E-15 ) ) ;
#15586=ADVANCED_FACE ( 'NONE', ( #10111 ), #14244, .T. ) ;
#15620=FACE_BOUND ( 'NONE', #17224, .T. ) ;
#15623=EDGE_CURVE ( 'NONE', #15456, #558, #3829, .T. ) ;
#15631=DIRECTION ( 'NONE',  ( 0.000000000000000000, -0.5000000000000011102, -0.8660254037844379305 ) ) ;
#15644=AXIS2_PLACEMENT_3D ( 'NONE', #3045, #12557, #3314 ) ;
#15673=ADVANCED_FACE ( 'NONE', ( #8684 ), #6999, .F. ) ;
#15693=CONICAL_SURFACE ( 'NONE', #8465, 2.055000000000000160, 0.7853981633974794763 ) ;
#15732=DIRECTION ( 'NONE',  ( 1.000000000000000000, 0.000000000000000000, 0.000000000000000000 ) ) ;
#15740=LINE ( 'NONE', #5652, #13039 ) ;
#15786=PLANE ( 'NONE',  #7561 ) ;
#15803=EDGE_CURVE ( 'NONE', #5445, #10572, #6314, .T. ) ;
#15812=DIRECTION ( 'NONE',  ( -1.000000000000000000, -0.000000000000000000, -0.000000000000000000 ) ) ;
#15817=CARTESIAN_POINT ( 'NONE',  ( 0.000000000000000000, 1.178949249685213863, -2.042000000000001148 ) ) ;
#15841=PLANE ( 'NONE',  #15343 ) ;
#15860=ORIENTED_EDGE ( 'NONE', *, *, #1481, .F. ) ;
#15863=CARTESIAN_POINT ( 'NONE',  ( 5.000000000000004441, 0.000000000000000000, 4.250000000000000000 ) ) ;
#15870=DIRECTION ( 'NONE',  ( -1.000000000000000000, -0.000000000000000000, -0.000000000000000000 ) ) ;
#15885=ORIENTED_EDGE ( 'NONE', *, *, #14794, .F. ) ;
#15892=VECTOR ( 'NONE', #12738, 1000.000000000000000 ) ;
#15916=DIRECTION ( 'NONE',  ( 0.000000000000000000, 0.000000000000000000, 1.000000000000000000 ) ) ;
#15936=DIRECTION ( 'NONE',  ( -1.000000000000000000, -0.000000000000000000, -0.000000000000000000 ) ) ;
#15937=ORIENTED_EDGE ( 'NONE', *, *, #4914, .T. ) ;
#15939=CARTESIAN_POINT ( 'NONE',  ( 2.500000000000000000, -2.357898499370431722, 2.818925648462311528E-15 ) ) ;
#15953=VERTEX_POINT ( 'NONE', #11160 ) ;
#16020=ORIENTED_EDGE ( 'NONE', *, *, #15089, .F. ) ;
#16036=DIRECTION ( 'NONE',  ( 0.000000000000000000, 0.000000000000000000, -1.000000000000000000 ) ) ;
#16044=CARTESIAN_POINT ( 'NONE',  ( 39.99999999999999289, 2.789133085058097101E-16, -2.055000000000000160 ) ) ;
#16059=DIRECTION ( 'NONE',  ( -1.000000000000000000, -0.000000000000000000, -0.000000000000000000 ) ) ;
#16074=CARTESIAN_POINT ( 'NONE',  ( 0.000000000000000000, -1.178949249685213863, 2.042000000000001148 ) ) ;
#16079=CYLINDRICAL_SURFACE ( 'NONE', #15081, 4.250000000000000000 ) ;
#16114=VERTEX_POINT ( 'NONE', #15541 ) ;
#16171=ORIENTED_EDGE ( 'NONE', *, *, #6062, .T. ) ;
#16213=EDGE_CURVE ( 'NONE', #16114, #1819, #16595, .T. ) ;
#16216=( NAMED_UNIT ( * ) PLANE_ANGLE_UNIT ( ) SI_UNIT ( $, .RADIAN. ) );
#16223=ORIENTED_EDGE ( 'NONE', *, *, #9120, .T. ) ;
#16308=CARTESIAN_POINT ( 'NONE',  ( 0.000000000000000000, 2.357898499370432166, -2.385244779468109755E-15 ) ) ;
#16375=PLANE ( 'NONE',  #8341 ) ;
#16394=CARTESIAN_POINT ( 'NONE',  ( 2.500000000000000000, 2.357898499370432166, -2.385244779468109755E-15 ) ) ;
#16445=VECTOR ( 'NONE', #13434, 1000.000000000000000 ) ;
#16472=EDGE_CURVE ( 'NONE', #2403, #12037, #3933, .T. ) ;
#16510=DIRECTION ( 'NONE',  ( 0.000000000000000000, 0.000000000000000000, 1.000000000000000000 ) ) ;
#16516=DIRECTION ( 'NONE',  ( 0.000000000000000000, 1.000000000000000000, -1.103561164596346103E-15 ) ) ;
#16534=CARTESIAN_POINT ( 'NONE',  ( 2.500000000000000000, -2.357898499370431722, 2.818925648462311528E-15 ) ) ;
#16558=DIRECTION ( 'NONE',  ( 1.000000000000000000, 0.000000000000000000, 0.000000000000000000 ) ) ;
#16563=ORIENTED_EDGE ( 'NONE', *, *, #4582, .T. ) ;
#16585=CIRCLE ( 'NONE', #1519, 4.250000000000000000 ) ;
#16595=CIRCLE ( 'NONE', #8784, 4.000000000000000000 ) ;
#16598=EDGE_CURVE ( 'NONE', #6324, #12037, #11324, .T. ) ;
#16603=CARTESIAN_POINT ( 'NONE',  ( 0.2500000000000002220, 5.204748896376250699E-16, -4.250000000000000000 ) ) ;
#16605=AXIS2_PLACEMENT_3D ( 'NONE', #15939, #6315, #17230 ) ;
#16607=EDGE_CURVE ( 'NONE', #9975, #2513, #15165, .T. ) ;
#16616=EDGE_LOOP ( 'NONE', ( #9947, #13480, #8510, #17948 ) ) ;
#16652=DIRECTION ( 'NONE',  ( 1.000000000000000000, 0.000000000000000000, 0.000000000000000000 ) ) ;
#16655=VERTEX_POINT ( 'NONE', #12133 ) ;
#16715=DIRECTION ( 'NONE',  ( -1.000000000000000000, -0.000000000000000000, -0.000000000000000000 ) ) ;
#16809=ORIENTED_EDGE ( 'NONE', *, *, #15161, .T. ) ;
#16840=CARTESIAN_POINT ( 'NONE',  ( 5.200000000000002842, 0.000000000000000000, 0.000000000000000000 ) ) ;
#16843=VECTOR ( 'NONE', #16516, 1000.000000000000000 ) ;
#16880=DIRECTION ( 'NONE',  ( -1.000000000000000000, -0.000000000000000000, -0.000000000000000000 ) ) ;
#16953=DIRECTION ( 'NONE',  ( -1.000000000000000000, -0.000000000000000000, -0.000000000000000000 ) ) ;
#16983=ORIENTED_EDGE ( 'NONE', *, *, #6062, .F. ) ;
#16987=CARTESIAN_POINT ( 'NONE',  ( 0.000000000000000000, 2.357898499370432166, -2.385244779468109755E-15 ) ) ;
#17003=FACE_OUTER_BOUND ( 'NONE', #17530, .T. ) ;
#17037=EDGE_CURVE ( 'NONE', #5445, #2513, #5803, .T. ) ;
#17080=CARTESIAN_POINT ( 'NONE',  ( 39.99999999999999289, 0.000000000000000000, 2.055000000000000160 ) ) ;
#17087=FACE_OUTER_BOUND ( 'NONE', #5114, .T. ) ;
#17104=AXIS2_PLACEMENT_3D ( 'NONE', #9039, #11744, #16036 ) ;
#17106=LINE ( 'NONE', #587, #17747 ) ;
#17111=SHAPE_DEFINITION_REPRESENTATION ( #15193, #3339 ) ;
#17185=VECTOR ( 'NONE', #10475, 1000.000000000000000 ) ;
#17224=EDGE_LOOP ( 'NONE', ( #4959, #4631, #14835, #7011, #5678, #6508 ) ) ;
#17230=DIRECTION ( 'NONE',  ( 0.000000000000000000, -0.4999999999999991118, 0.8660254037844390407 ) ) ;
#17232=EDGE_CURVE ( 'NONE', #11951, #15953, #14233, .T. ) ;
#17233=PLANE ( 'NONE',  #4305 ) ;
#17253=CARTESIAN_POINT ( 'NONE',  ( 2.500000000000000000, 1.768423874527825124, 1.020999999999998797 ) ) ;
#17268=VERTEX_POINT ( 'NONE', #13317 ) ;
#17289=CARTESIAN_POINT ( 'NONE',  ( 2.500000000000000000, -1.178949249685218081, -2.041999999999998039 ) ) ;
#17320=FILL_AREA_STYLE ('',( #5043 ) ) ;
#17324=DIRECTION ( 'NONE',  ( 0.000000000000000000, 1.224646799147353207E-16, 1.000000000000000000 ) ) ;
#17325=MANIFOLD_SOLID_BREP ( 'Hex', #312 ) ;
#17335=ORIENTED_EDGE ( 'NONE', *, *, #9303, .T. ) ;
#17357=ORIENTED_EDGE ( 'NONE', *, *, #9303, .F. ) ;
#17365=DIRECTION ( 'NONE',  ( 0.000000000000000000, 0.000000000000000000, 1.000000000000000000 ) ) ;
#17421=AXIS2_PLACEMENT_3D ( 'NONE', #17560, #8073, #16510 ) ;
#17451=VECTOR ( 'NONE', #2449, 1000.000000000000000 ) ;
#17481=CARTESIAN_POINT ( 'NONE',  ( 5.000000000000000888, 0.000000000000000000, 0.000000000000000000 ) ) ;
#17491=VECTOR ( 'NONE', #2387, 1000.000000000000114 ) ;
#17494=CARTESIAN_POINT ( 'NONE',  ( 39.55500000000002103, 0.000000000000000000, 0.000000000000000000 ) ) ;
#17522=( NAMED_UNIT ( * ) SI_UNIT ( $, .STERADIAN. ) SOLID_ANGLE_UNIT ( ) );
#17530=EDGE_LOOP ( 'NONE', ( #17805, #7227, #7376, #8894 ) ) ;
#17536=ORIENTED_EDGE ( 'NONE', *, *, #12545, .F. ) ;
#17560=CARTESIAN_POINT ( 'NONE',  ( -31.74999999999995737, 0.000000000000000000, 0.000000000000000000 ) ) ;
#17575=DIRECTION ( 'NONE',  ( 0.000000000000000000, 0.000000000000000000, 1.000000000000000000 ) ) ;
#17604=DIRECTION ( 'NONE',  ( -1.000000000000000000, -0.000000000000000000, -0.000000000000000000 ) ) ;
#17654=ORIENTED_EDGE ( 'NONE', *, *, #5987, .F. ) ;
#17672=FACE_BOUND ( 'NONE', #9708, .T. ) ;
#17674=VERTEX_POINT ( 'NONE', #17289 ) ;
#17675=CIRCLE ( 'NONE', #6350, 4.000000000000000000 ) ;
#17691=ADVANCED_FACE ( 'NONE', ( #8653 ), #4700, .F. ) ;
#17701=LINE ( 'NONE', #5223, #10196 ) ;
#17711=APPLICATION_CONTEXT ( 'automotive_design' ) ;
#17732=AXIS2_PLACEMENT_3D ( 'NONE', #17494, #5020, #15916 ) ;
#17737=DIRECTION ( 'NONE',  ( 0.000000000000000000, 0.000000000000000000, 1.000000000000000000 ) ) ;
#17747=VECTOR ( 'NONE', #8839, 1000.000000000000000 ) ;
#17752=CIRCLE ( 'NONE', #3834, 2.041999999999999815 ) ;
#17805=ORIENTED_EDGE ( 'NONE', *, *, #9380, .F. ) ;
#17898=CYLINDRICAL_SURFACE ( 'NONE', #17421, 4.250000000000000000 ) ;
#17948=ORIENTED_EDGE ( 'NONE', *, *, #11261, .F. ) ;
#17954=PRESENTATION_STYLE_ASSIGNMENT (( #10016 ) ) ;
ENDSEC;
END-ISO-10303-21;
